ISO-10303-21;
HEADER;
/* Generated by software containing ST-Developer
 * from STEP Tools, Inc. (www.steptools.com) 
 */

FILE_DESCRIPTION(
/* description */ ('Hand drill press frame (manual)'),
/* implementation_level */ '2;1');

FILE_NAME(
/* name */ 'Flat Washer - M6.step',
/* time_stamp */ '2026-10-28T03:25:28-07:00',
/* author */ (''),
/* organization */ (''),
/* preprocessor_version */ 'ST-DEVELOPER v20.2',
/* originating_system */ 'Autodesk Translation Framework v15.17.0.0',
/* authorisation */ '');

FILE_SCHEMA (('AUTOMOTIVE_DESIGN { 1 0 10303 214 3 1 1 }'));
ENDSEC;

DATA;
#10=MECHANICAL_DESIGN_GEOMETRIC_PRESENTATION_REPRESENTATION('',(#667),#33299);
#570=SHAPE_REPRESENTATION_RELATIONSHIP('SRR','None',#33532,#615);
#615=ADVANCED_BREP_SHAPE_REPRESENTATION('',(#718),#33294);
#667=STYLED_ITEM('',(#33821),#718);
#718=MANIFOLD_SOLID_BREP('Body1',#12686);
#881=FACE_BOUND('',#2839,.T.);
#882=FACE_BOUND('',#2841,.T.);
#1313=PLANE('',#14234);
#1314=PLANE('',#14235);
#1986=FACE_OUTER_BOUND('',#2836,.T.);
#1987=FACE_OUTER_BOUND('',#2837,.T.);
#1988=FACE_OUTER_BOUND('',#2838,.T.);
#1989=FACE_OUTER_BOUND('',#2840,.T.);
#2836=EDGE_LOOP('',(#11633,#11634,#11635,#11636));
#2837=EDGE_LOOP('',(#11637,#11638,#11639,#11640));
#2838=EDGE_LOOP('',(#11641));
#2839=EDGE_LOOP('',(#11642));
#2840=EDGE_LOOP('',(#11643));
#2841=EDGE_LOOP('',(#11644));
#3997=LINE('',#32961,#5162);
#3998=LINE('',#32967,#5163);
#5162=VECTOR('',#17564,0.32);
#5163=VECTOR('',#17571,0.6);
#5589=CIRCLE('',#14229,0.32);
#5590=CIRCLE('',#14230,0.32);
#5591=CIRCLE('',#14232,0.6);
#5592=CIRCLE('',#14233,0.6);
#6691=VERTEX_POINT('',#32958);
#6692=VERTEX_POINT('',#32960);
#6693=VERTEX_POINT('',#32964);
#6694=VERTEX_POINT('',#32966);
#8345=EDGE_CURVE('',#6691,#6691,#5589,.T.);
#8346=EDGE_CURVE('',#6691,#6692,#3997,.T.);
#8347=EDGE_CURVE('',#6692,#6692,#5590,.T.);
#8348=EDGE_CURVE('',#6693,#6693,#5591,.T.);
#8349=EDGE_CURVE('',#6693,#6694,#3998,.T.);
#8350=EDGE_CURVE('',#6694,#6694,#5592,.T.);
#11633=ORIENTED_EDGE('',*,*,#8345,.F.);
#11634=ORIENTED_EDGE('',*,*,#8346,.T.);
#11635=ORIENTED_EDGE('',*,*,#8347,.T.);
#11636=ORIENTED_EDGE('',*,*,#8346,.F.);
#11637=ORIENTED_EDGE('',*,*,#8348,.F.);
#11638=ORIENTED_EDGE('',*,*,#8349,.T.);
#11639=ORIENTED_EDGE('',*,*,#8350,.T.);
#11640=ORIENTED_EDGE('',*,*,#8349,.F.);
#11641=ORIENTED_EDGE('',*,*,#8348,.T.);
#11642=ORIENTED_EDGE('',*,*,#8345,.T.);
#11643=ORIENTED_EDGE('',*,*,#8350,.F.);
#11644=ORIENTED_EDGE('',*,*,#8347,.F.);
#11940=CYLINDRICAL_SURFACE('',#14228,0.32);
#11941=CYLINDRICAL_SURFACE('',#14231,0.6);
#12595=ADVANCED_FACE('',(#1986),#11940,.F.);
#12596=ADVANCED_FACE('',(#1987),#11941,.T.);
#12597=ADVANCED_FACE('',(#1988,#881),#1313,.T.);
#12598=ADVANCED_FACE('',(#1989,#882),#1314,.F.);
#12686=CLOSED_SHELL('',(#12595,#12596,#12597,#12598));
#14227=AXIS2_PLACEMENT_3D('',#32956,#17558,#17559);
#14228=AXIS2_PLACEMENT_3D('',#32957,#17560,#17561);
#14229=AXIS2_PLACEMENT_3D('',#32959,#17562,#17563);
#14230=AXIS2_PLACEMENT_3D('',#32962,#17565,#17566);
#14231=AXIS2_PLACEMENT_3D('',#32963,#17567,#17568);
#14232=AXIS2_PLACEMENT_3D('',#32965,#17569,#17570);
#14233=AXIS2_PLACEMENT_3D('',#32968,#17572,#17573);
#14234=AXIS2_PLACEMENT_3D('',#32969,#17574,#17575);
#14235=AXIS2_PLACEMENT_3D('',#32970,#17576,#17577);
#17558=DIRECTION('axis',(0.,0.,1.));
#17559=DIRECTION('refdir',(1.,0.,0.));
#17560=DIRECTION('center_axis',(0.,1.,0.));
#17561=DIRECTION('ref_axis',(1.,0.,0.));
#17562=DIRECTION('center_axis',(0.,-1.,0.));
#17563=DIRECTION('ref_axis',(1.,0.,0.));
#17564=DIRECTION('',(0.,-1.,0.));
#17565=DIRECTION('center_axis',(0.,-1.,0.));
#17566=DIRECTION('ref_axis',(1.,0.,0.));
#17567=DIRECTION('center_axis',(0.,1.,0.));
#17568=DIRECTION('ref_axis',(1.,0.,0.));
#17569=DIRECTION('center_axis',(0.,1.,0.));
#17570=DIRECTION('ref_axis',(1.,0.,0.));
#17571=DIRECTION('',(0.,-1.,0.));
#17572=DIRECTION('center_axis',(0.,1.,0.));
#17573=DIRECTION('ref_axis',(1.,0.,0.));
#17574=DIRECTION('center_axis',(0.,1.,0.));
#17575=DIRECTION('ref_axis',(1.,0.,0.));
#17576=DIRECTION('center_axis',(0.,1.,0.));
#17577=DIRECTION('ref_axis',(1.,0.,0.));
#32956=CARTESIAN_POINT('',(0.,0.,0.));
#32957=CARTESIAN_POINT('Origin',(0.,0.,0.));
#32958=CARTESIAN_POINT('',(-0.32,0.16,3.91886975727153E-17));
#32959=CARTESIAN_POINT('Origin',(0.,0.16,0.));
#32960=CARTESIAN_POINT('',(-0.32,0.,3.91886975727153E-17));
#32961=CARTESIAN_POINT('',(-0.32,0.,3.91886975727153E-17));
#32962=CARTESIAN_POINT('Origin',(0.,0.,0.));
#32963=CARTESIAN_POINT('Origin',(0.,0.,0.));
#32964=CARTESIAN_POINT('',(-0.6,0.16,7.34788079488412E-17));
#32965=CARTESIAN_POINT('Origin',(0.,0.16,0.));
#32966=CARTESIAN_POINT('',(-0.6,0.,7.34788079488412E-17));
#32967=CARTESIAN_POINT('',(-0.6,0.,7.34788079488412E-17));
#32968=CARTESIAN_POINT('Origin',(0.,0.,0.));
#32969=CARTESIAN_POINT('Origin',(0.,0.16,0.));
#32970=CARTESIAN_POINT('Origin',(0.,0.,0.));
#33242=UNCERTAINTY_MEASURE_WITH_UNIT(LENGTH_MEASURE(0.001),#33300,
'DISTANCE_ACCURACY_VALUE',
'Maximum model space distance between geometric entities at asserted c
onnectivities');
#33247=UNCERTAINTY_MEASURE_WITH_UNIT(LENGTH_MEASURE(0.001),#33300,
'DISTANCE_ACCURACY_VALUE',
'Maximum model space distance between geometric entities at asserted c
onnectivities');
#33294=(
GEOMETRIC_REPRESENTATION_CONTEXT(3)
GLOBAL_UNCERTAINTY_ASSIGNED_CONTEXT((#33242))
GLOBAL_UNIT_ASSIGNED_CONTEXT((#33300,#33302,#33303))
REPRESENTATION_CONTEXT('','3D')
);
#33299=(
GEOMETRIC_REPRESENTATION_CONTEXT(3)
GLOBAL_UNCERTAINTY_ASSIGNED_CONTEXT((#33247))
GLOBAL_UNIT_ASSIGNED_CONTEXT((#33300,#33302,#33303))
REPRESENTATION_CONTEXT('','3D')
);
#33300=(
LENGTH_UNIT()
NAMED_UNIT(*)
SI_UNIT(.CENTI.,.METRE.)
);
#33302=(
NAMED_UNIT(*)
PLANE_ANGLE_UNIT()
SI_UNIT($,.RADIAN.)
);
#33303=(
NAMED_UNIT(*)
SI_UNIT($,.STERADIAN.)
SOLID_ANGLE_UNIT()
);
#33350=SHAPE_DEFINITION_REPRESENTATION(#33412,#33532);
#33412=PRODUCT_DEFINITION_SHAPE('',$,#33584);
#33532=SHAPE_REPRESENTATION('',(#14227),#33294);
#33537=PRODUCT_DEFINITION_CONTEXT('part definition',#33692,'design');
#33584=PRODUCT_DEFINITION('Flat Washer - M6','Flat Washer - M6',#33635,
#33537);
#33635=PRODUCT_DEFINITION_FORMATION('',$,#33740);
#33692=APPLICATION_CONTEXT(
'Core Data for Automotive Mechanical Design Process');
#33693=PRODUCT_CONTEXT('part definition',#33692,'mechanical');
#33740=PRODUCT('Flat Washer - M6','Flat Washer - M6','Flat Washer - M6',
(#33693));
#33815=COLOUR_RGB('Black',0.12,0.14,0.17);
#33816=FILL_AREA_STYLE_COLOUR('',#33815);
#33817=FILL_AREA_STYLE('',(#33816));
#33818=SURFACE_STYLE_FILL_AREA(#33817);
#33819=SURFACE_SIDE_STYLE('',(#33818));
#33820=SURFACE_STYLE_USAGE(.BOTH.,#33819);
#33821=PRESENTATION_STYLE_ASSIGNMENT((#33820));
ENDSEC;
END-ISO-10303-21;
